ISO-10303-21;
HEADER;
/* Generated by software containing ST-Developer
 * from STEP Tools, Inc. (www.steptools.com) 
 */

FILE_DESCRIPTION(
/* description */ ('Drill jig with bushing plate'),
/* implementation_level */ '2;1');

FILE_NAME(
/* name */ 'M5x14 Cap Screw.step',
/* time_stamp */ '2026-10-27T10:51:08-07:00',
/* author */ (''),
/* organization */ (''),
/* preprocessor_version */ 'ST-DEVELOPER v20.2',
/* originating_system */ 'Autodesk Translation Framework v15.17.0.0',
/* authorisation */ '');

FILE_SCHEMA (('AUTOMOTIVE_DESIGN { 1 0 10303 214 3 1 1 }'));
ENDSEC;

DATA;
#10=MECHANICAL_DESIGN_GEOMETRIC_PRESENTATION_REPRESENTATION('',(#238),#6638);
#163=CONICAL_SURFACE('',#4144,0.4,0.785398163397448);
#164=CONICAL_SURFACE('',#4148,0.41,0.785398163397448);
#165=CONICAL_SURFACE('',#4152,0.26,0.463647609000806);
#169=ORIENTED_CLOSED_SHELL('',*,#3605,.F.);
#171=BREP_WITH_VOIDS('Body1',#3606,(#169));
#190=SHAPE_REPRESENTATION_RELATIONSHIP('SRR','None',#6754,#214);
#214=ADVANCED_BREP_SHAPE_REPRESENTATION('',(#171),#6627);
#238=STYLED_ITEM('',(#6950),#171);
#343=FACE_BOUND('',#926,.T.);
#442=PLANE('',#4132);
#443=PLANE('',#4133);
#444=PLANE('',#4134);
#445=PLANE('',#4135);
#446=PLANE('',#4136);
#447=PLANE('',#4137);
#448=PLANE('',#4138);
#449=PLANE('',#4139);
#450=PLANE('',#4140);
#451=PLANE('',#4142);
#452=PLANE('',#4150);
#624=FACE_OUTER_BOUND('',#912,.T.);
#625=FACE_OUTER_BOUND('',#913,.T.);
#626=FACE_OUTER_BOUND('',#914,.T.);
#627=FACE_OUTER_BOUND('',#915,.T.);
#628=FACE_OUTER_BOUND('',#916,.T.);
#629=FACE_OUTER_BOUND('',#917,.T.);
#630=FACE_OUTER_BOUND('',#918,.T.);
#631=FACE_OUTER_BOUND('',#919,.T.);
#632=FACE_OUTER_BOUND('',#920,.T.);
#633=FACE_OUTER_BOUND('',#921,.T.);
#634=FACE_OUTER_BOUND('',#922,.T.);
#635=FACE_OUTER_BOUND('',#923,.T.);
#636=FACE_OUTER_BOUND('',#924,.T.);
#637=FACE_OUTER_BOUND('',#925,.T.);
#638=FACE_OUTER_BOUND('',#927,.T.);
#639=FACE_OUTER_BOUND('',#928,.T.);
#912=EDGE_LOOP('',(#2939,#2940,#2941,#2942));
#913=EDGE_LOOP('',(#2943,#2944,#2945,#2946));
#914=EDGE_LOOP('',(#2947,#2948,#2949,#2950));
#915=EDGE_LOOP('',(#2951,#2952,#2953,#2954));
#916=EDGE_LOOP('',(#2955,#2956,#2957,#2958));
#917=EDGE_LOOP('',(#2959,#2960,#2961,#2962));
#918=EDGE_LOOP('',(#2963,#2964,#2965,#2966,#2967,#2968));
#919=EDGE_LOOP('',(#2969,#2970,#2971,#2972,#2973,#2974));
#920=EDGE_LOOP('',(#2975));
#921=EDGE_LOOP('',(#2976));
#922=EDGE_LOOP('',(#2977,#2978,#2979,#2980));
#923=EDGE_LOOP('',(#2981,#2982,#2983,#2984));
#924=EDGE_LOOP('',(#2985,#2986,#2987,#2988));
#925=EDGE_LOOP('',(#2989));
#926=EDGE_LOOP('',(#2990));
#927=EDGE_LOOP('',(#2991,#2992,#2993,#2994));
#928=EDGE_LOOP('',(#2995,#2996,#2997,#2998));
#1169=LINE('',#6147,#1430);
#1170=LINE('',#6149,#1431);
#1171=LINE('',#6151,#1432);
#1172=LINE('',#6152,#1433);
#1173=LINE('',#6155,#1434);
#1174=LINE('',#6157,#1435);
#1175=LINE('',#6158,#1436);
#1176=LINE('',#6161,#1437);
#1177=LINE('',#6163,#1438);
#1178=LINE('',#6164,#1439);
#1179=LINE('',#6167,#1440);
#1180=LINE('',#6169,#1441);
#1181=LINE('',#6170,#1442);
#1182=LINE('',#6173,#1443);
#1183=LINE('',#6175,#1444);
#1184=LINE('',#6176,#1445);
#1185=LINE('',#6178,#1446);
#1186=LINE('',#6179,#1447);
#1187=LINE('',#6191,#1448);
#1188=LINE('',#6195,#1449);
#1189=LINE('',#6199,#1450);
#1190=LINE('',#6206,#1451);
#1191=LINE('',#6208,#1452);
#1430=VECTOR('',#4972,1.);
#1431=VECTOR('',#4973,1.);
#1432=VECTOR('',#4974,1.);
#1433=VECTOR('',#4975,1.);
#1434=VECTOR('',#4978,1.);
#1435=VECTOR('',#4979,1.);
#1436=VECTOR('',#4980,1.);
#1437=VECTOR('',#4983,1.);
#1438=VECTOR('',#4984,1.);
#1439=VECTOR('',#4985,1.);
#1440=VECTOR('',#4988,1.);
#1441=VECTOR('',#4989,1.);
#1442=VECTOR('',#4990,1.);
#1443=VECTOR('',#4993,1.);
#1444=VECTOR('',#4994,1.);
#1445=VECTOR('',#4995,1.);
#1446=VECTOR('',#4998,1.);
#1447=VECTOR('',#4999,1.);
#1448=VECTOR('',#5016,0.4);
#1449=VECTOR('',#5021,0.425);
#1450=VECTOR('',#5026,0.41);
#1451=VECTOR('',#5035,0.26);
#1452=VECTOR('',#5038,0.25);
#1662=CIRCLE('',#4141,0.24505);
#1663=CIRCLE('',#4143,0.375);
#1664=CIRCLE('',#4145,0.425);
#1665=CIRCLE('',#4147,0.425);
#1666=CIRCLE('',#4149,0.395);
#1667=CIRCLE('',#4151,0.27);
#1668=CIRCLE('',#4153,0.24505);
#1888=VERTEX_POINT('',#6145);
#1889=VERTEX_POINT('',#6146);
#1890=VERTEX_POINT('',#6148);
#1891=VERTEX_POINT('',#6150);
#1892=VERTEX_POINT('',#6154);
#1893=VERTEX_POINT('',#6156);
#1894=VERTEX_POINT('',#6160);
#1895=VERTEX_POINT('',#6162);
#1896=VERTEX_POINT('',#6166);
#1897=VERTEX_POINT('',#6168);
#1898=VERTEX_POINT('',#6172);
#1899=VERTEX_POINT('',#6174);
#1900=VERTEX_POINT('',#6183);
#1901=VERTEX_POINT('',#6186);
#1902=VERTEX_POINT('',#6189);
#1903=VERTEX_POINT('',#6193);
#1904=VERTEX_POINT('',#6197);
#1905=VERTEX_POINT('',#6201);
#1906=VERTEX_POINT('',#6204);
#2257=EDGE_CURVE('',#1888,#1889,#1169,.T.);
#2258=EDGE_CURVE('',#1889,#1890,#1170,.T.);
#2259=EDGE_CURVE('',#1890,#1891,#1171,.T.);
#2260=EDGE_CURVE('',#1888,#1891,#1172,.T.);
#2261=EDGE_CURVE('',#1889,#1892,#1173,.T.);
#2262=EDGE_CURVE('',#1892,#1893,#1174,.T.);
#2263=EDGE_CURVE('',#1893,#1890,#1175,.T.);
#2264=EDGE_CURVE('',#1892,#1894,#1176,.T.);
#2265=EDGE_CURVE('',#1894,#1895,#1177,.T.);
#2266=EDGE_CURVE('',#1895,#1893,#1178,.T.);
#2267=EDGE_CURVE('',#1894,#1896,#1179,.T.);
#2268=EDGE_CURVE('',#1896,#1897,#1180,.T.);
#2269=EDGE_CURVE('',#1897,#1895,#1181,.T.);
#2270=EDGE_CURVE('',#1896,#1898,#1182,.T.);
#2271=EDGE_CURVE('',#1898,#1899,#1183,.T.);
#2272=EDGE_CURVE('',#1899,#1897,#1184,.T.);
#2273=EDGE_CURVE('',#1898,#1888,#1185,.T.);
#2274=EDGE_CURVE('',#1891,#1899,#1186,.T.);
#2275=EDGE_CURVE('',#1900,#1900,#1662,.T.);
#2276=EDGE_CURVE('',#1901,#1901,#1663,.T.);
#2277=EDGE_CURVE('',#1902,#1902,#1664,.T.);
#2278=EDGE_CURVE('',#1902,#1901,#1187,.T.);
#2279=EDGE_CURVE('',#1903,#1903,#1665,.T.);
#2280=EDGE_CURVE('',#1903,#1902,#1188,.T.);
#2281=EDGE_CURVE('',#1904,#1904,#1666,.T.);
#2282=EDGE_CURVE('',#1904,#1903,#1189,.T.);
#2283=EDGE_CURVE('',#1905,#1905,#1667,.T.);
#2284=EDGE_CURVE('',#1906,#1906,#1668,.F.);
#2285=EDGE_CURVE('',#1906,#1905,#1190,.T.);
#2286=EDGE_CURVE('',#1900,#1906,#1191,.T.);
#2939=ORIENTED_EDGE('',*,*,#2257,.T.);
#2940=ORIENTED_EDGE('',*,*,#2258,.T.);
#2941=ORIENTED_EDGE('',*,*,#2259,.T.);
#2942=ORIENTED_EDGE('',*,*,#2260,.F.);
#2943=ORIENTED_EDGE('',*,*,#2261,.T.);
#2944=ORIENTED_EDGE('',*,*,#2262,.T.);
#2945=ORIENTED_EDGE('',*,*,#2263,.T.);
#2946=ORIENTED_EDGE('',*,*,#2258,.F.);
#2947=ORIENTED_EDGE('',*,*,#2264,.T.);
#2948=ORIENTED_EDGE('',*,*,#2265,.T.);
#2949=ORIENTED_EDGE('',*,*,#2266,.T.);
#2950=ORIENTED_EDGE('',*,*,#2262,.F.);
#2951=ORIENTED_EDGE('',*,*,#2267,.T.);
#2952=ORIENTED_EDGE('',*,*,#2268,.T.);
#2953=ORIENTED_EDGE('',*,*,#2269,.T.);
#2954=ORIENTED_EDGE('',*,*,#2265,.F.);
#2955=ORIENTED_EDGE('',*,*,#2270,.T.);
#2956=ORIENTED_EDGE('',*,*,#2271,.T.);
#2957=ORIENTED_EDGE('',*,*,#2272,.T.);
#2958=ORIENTED_EDGE('',*,*,#2268,.F.);
#2959=ORIENTED_EDGE('',*,*,#2273,.T.);
#2960=ORIENTED_EDGE('',*,*,#2260,.T.);
#2961=ORIENTED_EDGE('',*,*,#2274,.T.);
#2962=ORIENTED_EDGE('',*,*,#2271,.F.);
#2963=ORIENTED_EDGE('',*,*,#2273,.F.);
#2964=ORIENTED_EDGE('',*,*,#2270,.F.);
#2965=ORIENTED_EDGE('',*,*,#2267,.F.);
#2966=ORIENTED_EDGE('',*,*,#2264,.F.);
#2967=ORIENTED_EDGE('',*,*,#2261,.F.);
#2968=ORIENTED_EDGE('',*,*,#2257,.F.);
#2969=ORIENTED_EDGE('',*,*,#2274,.F.);
#2970=ORIENTED_EDGE('',*,*,#2259,.F.);
#2971=ORIENTED_EDGE('',*,*,#2263,.F.);
#2972=ORIENTED_EDGE('',*,*,#2266,.F.);
#2973=ORIENTED_EDGE('',*,*,#2269,.F.);
#2974=ORIENTED_EDGE('',*,*,#2272,.F.);
#2975=ORIENTED_EDGE('',*,*,#2275,.F.);
#2976=ORIENTED_EDGE('',*,*,#2276,.F.);
#2977=ORIENTED_EDGE('',*,*,#2277,.F.);
#2978=ORIENTED_EDGE('',*,*,#2278,.T.);
#2979=ORIENTED_EDGE('',*,*,#2276,.T.);
#2980=ORIENTED_EDGE('',*,*,#2278,.F.);
#2981=ORIENTED_EDGE('',*,*,#2279,.F.);
#2982=ORIENTED_EDGE('',*,*,#2280,.T.);
#2983=ORIENTED_EDGE('',*,*,#2277,.T.);
#2984=ORIENTED_EDGE('',*,*,#2280,.F.);
#2985=ORIENTED_EDGE('',*,*,#2281,.F.);
#2986=ORIENTED_EDGE('',*,*,#2282,.T.);
#2987=ORIENTED_EDGE('',*,*,#2279,.T.);
#2988=ORIENTED_EDGE('',*,*,#2282,.F.);
#2989=ORIENTED_EDGE('',*,*,#2281,.T.);
#2990=ORIENTED_EDGE('',*,*,#2283,.F.);
#2991=ORIENTED_EDGE('',*,*,#2284,.F.);
#2992=ORIENTED_EDGE('',*,*,#2285,.T.);
#2993=ORIENTED_EDGE('',*,*,#2283,.T.);
#2994=ORIENTED_EDGE('',*,*,#2285,.F.);
#2995=ORIENTED_EDGE('',*,*,#2275,.T.);
#2996=ORIENTED_EDGE('',*,*,#2286,.T.);
#2997=ORIENTED_EDGE('',*,*,#2284,.T.);
#2998=ORIENTED_EDGE('',*,*,#2286,.F.);
#3350=CYLINDRICAL_SURFACE('',#4146,0.425);
#3351=CYLINDRICAL_SURFACE('',#4154,0.24505);
#3499=ADVANCED_FACE('',(#624),#442,.F.);
#3500=ADVANCED_FACE('',(#625),#443,.F.);
#3501=ADVANCED_FACE('',(#626),#444,.F.);
#3502=ADVANCED_FACE('',(#627),#445,.F.);
#3503=ADVANCED_FACE('',(#628),#446,.F.);
#3504=ADVANCED_FACE('',(#629),#447,.F.);
#3505=ADVANCED_FACE('',(#630),#448,.F.);
#3506=ADVANCED_FACE('',(#631),#449,.F.);
#3507=ADVANCED_FACE('',(#632),#450,.F.);
#3508=ADVANCED_FACE('',(#633),#451,.T.);
#3509=ADVANCED_FACE('',(#634),#163,.T.);
#3510=ADVANCED_FACE('',(#635),#3350,.T.);
#3511=ADVANCED_FACE('',(#636),#164,.T.);
#3512=ADVANCED_FACE('',(#637,#343),#452,.T.);
#3513=ADVANCED_FACE('',(#638),#165,.T.);
#3514=ADVANCED_FACE('',(#639),#3351,.T.);
#3605=CLOSED_SHELL('',(#3499,#3500,#3501,#3502,#3503,#3504,#3505,#3506));
#3606=CLOSED_SHELL('',(#3507,#3508,#3509,#3510,#3511,#3512,#3513,#3514));
#4131=AXIS2_PLACEMENT_3D('',#6143,#4968,#4969);
#4132=AXIS2_PLACEMENT_3D('',#6144,#4970,#4971);
#4133=AXIS2_PLACEMENT_3D('',#6153,#4976,#4977);
#4134=AXIS2_PLACEMENT_3D('',#6159,#4981,#4982);
#4135=AXIS2_PLACEMENT_3D('',#6165,#4986,#4987);
#4136=AXIS2_PLACEMENT_3D('',#6171,#4991,#4992);
#4137=AXIS2_PLACEMENT_3D('',#6177,#4996,#4997);
#4138=AXIS2_PLACEMENT_3D('',#6180,#5000,#5001);
#4139=AXIS2_PLACEMENT_3D('',#6181,#5002,#5003);
#4140=AXIS2_PLACEMENT_3D('',#6182,#5004,#5005);
#4141=AXIS2_PLACEMENT_3D('',#6184,#5006,#5007);
#4142=AXIS2_PLACEMENT_3D('',#6185,#5008,#5009);
#4143=AXIS2_PLACEMENT_3D('',#6187,#5010,#5011);
#4144=AXIS2_PLACEMENT_3D('',#6188,#5012,#5013);
#4145=AXIS2_PLACEMENT_3D('',#6190,#5014,#5015);
#4146=AXIS2_PLACEMENT_3D('',#6192,#5017,#5018);
#4147=AXIS2_PLACEMENT_3D('',#6194,#5019,#5020);
#4148=AXIS2_PLACEMENT_3D('',#6196,#5022,#5023);
#4149=AXIS2_PLACEMENT_3D('',#6198,#5024,#5025);
#4150=AXIS2_PLACEMENT_3D('',#6200,#5027,#5028);
#4151=AXIS2_PLACEMENT_3D('',#6202,#5029,#5030);
#4152=AXIS2_PLACEMENT_3D('',#6203,#5031,#5032);
#4153=AXIS2_PLACEMENT_3D('',#6205,#5033,#5034);
#4154=AXIS2_PLACEMENT_3D('',#6207,#5036,#5037);
#4968=DIRECTION('axis',(0.,0.,1.));
#4969=DIRECTION('refdir',(1.,0.,0.));
#4970=DIRECTION('center_axis',(0.866025403784439,0.,-0.5));
#4971=DIRECTION('ref_axis',(0.5,0.,0.866025403784439));
#4972=DIRECTION('',(-0.5,0.,-0.866025403784439));
#4973=DIRECTION('',(0.,-1.,0.));
#4974=DIRECTION('',(0.5,0.,0.866025403784439));
#4975=DIRECTION('',(0.,-1.,0.));
#4976=DIRECTION('center_axis',(1.20185167898973E-16,0.,-1.));
#4977=DIRECTION('ref_axis',(1.,0.,1.20185167898973E-16));
#4978=DIRECTION('',(-1.,0.,-1.20185167898973E-16));
#4979=DIRECTION('',(0.,-1.,0.));
#4980=DIRECTION('',(1.,0.,1.20185167898973E-16));
#4981=DIRECTION('center_axis',(-0.866025403784439,0.,-0.5));
#4982=DIRECTION('ref_axis',(0.5,0.,-0.866025403784439));
#4983=DIRECTION('',(-0.5,0.,0.866025403784439));
#4984=DIRECTION('',(0.,-1.,0.));
#4985=DIRECTION('',(0.5,0.,-0.866025403784439));
#4986=DIRECTION('center_axis',(-0.866025403784439,0.,0.5));
#4987=DIRECTION('ref_axis',(-0.5,0.,-0.866025403784439));
#4988=DIRECTION('',(0.5,0.,0.866025403784439));
#4989=DIRECTION('',(0.,-1.,0.));
#4990=DIRECTION('',(-0.5,0.,-0.866025403784439));
#4991=DIRECTION('center_axis',(-2.40370335797945E-16,0.,1.));
#4992=DIRECTION('ref_axis',(-1.,0.,-2.40370335797945E-16));
#4993=DIRECTION('',(1.,0.,2.40370335797945E-16));
#4994=DIRECTION('',(0.,-1.,0.));
#4995=DIRECTION('',(-1.,0.,-2.40370335797945E-16));
#4996=DIRECTION('center_axis',(0.866025403784439,0.,0.5));
#4997=DIRECTION('ref_axis',(-0.5,0.,0.866025403784439));
#4998=DIRECTION('',(0.5,0.,-0.866025403784439));
#4999=DIRECTION('',(-0.5,0.,0.866025403784439));
#5000=DIRECTION('center_axis',(0.,1.,0.));
#5001=DIRECTION('ref_axis',(1.,0.,0.));
#5002=DIRECTION('center_axis',(0.,-1.,0.));
#5003=DIRECTION('ref_axis',(0.,0.,-1.));
#5004=DIRECTION('center_axis',(0.,1.,0.));
#5005=DIRECTION('ref_axis',(1.,0.,0.));
#5006=DIRECTION('center_axis',(0.,1.,0.));
#5007=DIRECTION('ref_axis',(1.,0.,0.));
#5008=DIRECTION('center_axis',(0.,1.,0.));
#5009=DIRECTION('ref_axis',(0.,0.,1.));
#5010=DIRECTION('center_axis',(0.,-1.,0.));
#5011=DIRECTION('ref_axis',(1.,0.,0.));
#5012=DIRECTION('center_axis',(0.,-1.,0.));
#5013=DIRECTION('ref_axis',(1.,0.,0.));
#5014=DIRECTION('center_axis',(0.,-1.,0.));
#5015=DIRECTION('ref_axis',(1.,0.,0.));
#5016=DIRECTION('',(0.707106781186548,0.707106781186547,8.65956056235493E-17));
#5017=DIRECTION('center_axis',(0.,-1.,0.));
#5018=DIRECTION('ref_axis',(1.,0.,0.));
#5019=DIRECTION('center_axis',(0.,-1.,0.));
#5020=DIRECTION('ref_axis',(1.,0.,0.));
#5021=DIRECTION('',(0.,1.,0.));
#5022=DIRECTION('center_axis',(0.,1.,0.));
#5023=DIRECTION('ref_axis',(1.,0.,0.));
#5024=DIRECTION('center_axis',(0.,-1.,0.));
#5025=DIRECTION('ref_axis',(1.,0.,0.));
#5026=DIRECTION('',(-0.707106781186547,0.707106781186548,-8.65956056235493E-17));
#5027=DIRECTION('center_axis',(0.,-1.,0.));
#5028=DIRECTION('ref_axis',(0.,0.,-1.));
#5029=DIRECTION('center_axis',(0.,-1.,0.));
#5030=DIRECTION('ref_axis',(1.,0.,0.));
#5031=DIRECTION('center_axis',(0.,1.,0.));
#5032=DIRECTION('ref_axis',(1.,0.,0.));
#5033=DIRECTION('center_axis',(0.,1.,0.));
#5034=DIRECTION('ref_axis',(1.,0.,0.));
#5035=DIRECTION('',(-0.447213595499958,0.894427190999916,-5.47678698264203E-17));
#5036=DIRECTION('center_axis',(0.,-1.,0.));
#5037=DIRECTION('ref_axis',(1.,0.,0.));
#5038=DIRECTION('',(0.,1.,0.));
#6143=CARTESIAN_POINT('',(0.,0.,0.));
#6144=CARTESIAN_POINT('Origin',(0.115470053837925,-0.5,-0.2));
#6145=CARTESIAN_POINT('',(0.23094010767585,-0.5,0.));
#6146=CARTESIAN_POINT('',(0.115470053837925,-0.5,-0.2));
#6147=CARTESIAN_POINT('',(0.23094010767585,-0.5,0.));
#6148=CARTESIAN_POINT('',(0.115470053837925,-0.8,-0.2));
#6149=CARTESIAN_POINT('',(0.115470053837925,-0.5,-0.2));
#6150=CARTESIAN_POINT('',(0.23094010767585,-0.8,0.));
#6151=CARTESIAN_POINT('',(0.23094010767585,-0.8,0.));
#6152=CARTESIAN_POINT('',(0.23094010767585,-0.5,0.));
#6153=CARTESIAN_POINT('Origin',(-0.115470053837925,-0.5,-0.2));
#6154=CARTESIAN_POINT('',(-0.115470053837925,-0.5,-0.2));
#6155=CARTESIAN_POINT('',(0.115470053837925,-0.5,-0.2));
#6156=CARTESIAN_POINT('',(-0.115470053837925,-0.8,-0.2));
#6157=CARTESIAN_POINT('',(-0.115470053837925,-0.5,-0.2));
#6158=CARTESIAN_POINT('',(0.115470053837925,-0.8,-0.2));
#6159=CARTESIAN_POINT('Origin',(-0.23094010767585,-0.5,-2.77555756156289E-17));
#6160=CARTESIAN_POINT('',(-0.23094010767585,-0.5,-2.82820063659975E-17));
#6161=CARTESIAN_POINT('',(-0.115470053837925,-0.5,-0.2));
#6162=CARTESIAN_POINT('',(-0.23094010767585,-0.8,-2.77555756156289E-17));
#6163=CARTESIAN_POINT('',(-0.23094010767585,-0.5,-2.82820063659975E-17));
#6164=CARTESIAN_POINT('',(-0.115470053837925,-0.8,-0.2));
#6165=CARTESIAN_POINT('Origin',(-0.115470053837925,-0.5,0.2));
#6166=CARTESIAN_POINT('',(-0.115470053837925,-0.5,0.2));
#6167=CARTESIAN_POINT('',(-0.23094010767585,-0.5,-2.82820063659975E-17));
#6168=CARTESIAN_POINT('',(-0.115470053837925,-0.8,0.2));
#6169=CARTESIAN_POINT('',(-0.115470053837925,-0.5,0.2));
#6170=CARTESIAN_POINT('',(-0.23094010767585,-0.8,-2.82820063659975E-17));
#6171=CARTESIAN_POINT('Origin',(0.115470053837925,-0.5,0.2));
#6172=CARTESIAN_POINT('',(0.115470053837925,-0.5,0.2));
#6173=CARTESIAN_POINT('',(-0.115470053837925,-0.5,0.2));
#6174=CARTESIAN_POINT('',(0.115470053837925,-0.8,0.2));
#6175=CARTESIAN_POINT('',(0.115470053837925,-0.5,0.2));
#6176=CARTESIAN_POINT('',(-0.115470053837925,-0.8,0.2));
#6177=CARTESIAN_POINT('Origin',(0.23094010767585,-0.5,0.));
#6178=CARTESIAN_POINT('',(0.115470053837925,-0.5,0.2));
#6179=CARTESIAN_POINT('',(0.115470053837925,-0.8,0.2));
#6180=CARTESIAN_POINT('Origin',(0.,-0.5,0.));
#6181=CARTESIAN_POINT('Origin',(0.,-0.8,0.));
#6182=CARTESIAN_POINT('Origin',(0.,-1.4,0.));
#6183=CARTESIAN_POINT('',(-0.24505,-1.4,3.00099698131059E-17));
#6184=CARTESIAN_POINT('Origin',(0.,-1.4,0.));
#6185=CARTESIAN_POINT('Origin',(0.375,0.5,0.));
#6186=CARTESIAN_POINT('',(-0.375,0.5,-4.59242549680257E-17));
#6187=CARTESIAN_POINT('Origin',(0.,0.5,0.));
#6188=CARTESIAN_POINT('Origin',(0.,0.475,0.));
#6189=CARTESIAN_POINT('',(-0.425,0.45,-5.20474889637625E-17));
#6190=CARTESIAN_POINT('Origin',(0.,0.45,0.));
#6191=CARTESIAN_POINT('',(-0.4,0.475,-4.89858719658941E-17));
#6192=CARTESIAN_POINT('Origin',(0.,0.24,0.));
#6193=CARTESIAN_POINT('',(-0.425,0.0299999999999998,-5.20474889637625E-17));
#6194=CARTESIAN_POINT('Origin',(0.,0.0299999999999998,0.));
#6195=CARTESIAN_POINT('',(-0.425,0.24,-5.20474889637625E-17));
#6196=CARTESIAN_POINT('Origin',(0.,0.0150000000000001,0.));
#6197=CARTESIAN_POINT('',(-0.395,4.85722573273506E-17,-4.83735485663204E-17));
#6198=CARTESIAN_POINT('Origin',(0.,0.,0.));
#6199=CARTESIAN_POINT('',(-0.41,0.0150000000000001,-5.02105187650415E-17));
#6200=CARTESIAN_POINT('Origin',(0.27,0.,0.));
#6201=CARTESIAN_POINT('',(-0.27,0.,-3.30654635769785E-17));
#6202=CARTESIAN_POINT('Origin',(0.,0.,0.));
#6203=CARTESIAN_POINT('Origin',(0.,-0.02,0.));
#6204=CARTESIAN_POINT('',(-0.24505,-0.0498999999999999,3.00099698131059E-17));
#6205=CARTESIAN_POINT('Origin',(0.,-0.0498999999999999,0.));
#6206=CARTESIAN_POINT('',(-0.26,-0.02,-3.18408167778312E-17));
#6207=CARTESIAN_POINT('Origin',(0.,-0.995,0.));
#6208=CARTESIAN_POINT('',(-0.24505,-0.995,-3.00099698131059E-17));
#6598=UNCERTAINTY_MEASURE_WITH_UNIT(LENGTH_MEASURE(0.001),#6639,
'DISTANCE_ACCURACY_VALUE',
'Maximum model space distance between geometric entities at asserted c
onnectivities');
#6609=UNCERTAINTY_MEASURE_WITH_UNIT(LENGTH_MEASURE(0.001),#6639,
'DISTANCE_ACCURACY_VALUE',
'Maximum model space distance between geometric entities at asserted c
onnectivities');
#6627=(
GEOMETRIC_REPRESENTATION_CONTEXT(3)
GLOBAL_UNCERTAINTY_ASSIGNED_CONTEXT((#6598))
GLOBAL_UNIT_ASSIGNED_CONTEXT((#6639,#6641,#6642))
REPRESENTATION_CONTEXT('','3D')
);
#6638=(
GEOMETRIC_REPRESENTATION_CONTEXT(3)
GLOBAL_UNCERTAINTY_ASSIGNED_CONTEXT((#6609))
GLOBAL_UNIT_ASSIGNED_CONTEXT((#6639,#6641,#6642))
REPRESENTATION_CONTEXT('','3D')
);
#6639=(
LENGTH_UNIT()
NAMED_UNIT(*)
SI_UNIT(.CENTI.,.METRE.)
);
#6641=(
NAMED_UNIT(*)
PLANE_ANGLE_UNIT()
SI_UNIT($,.RADIAN.)
);
#6642=(
NAMED_UNIT(*)
SI_UNIT($,.STERADIAN.)
SOLID_ANGLE_UNIT()
);
#6660=SHAPE_DEFINITION_REPRESENTATION(#6688,#6754);
#6688=PRODUCT_DEFINITION_SHAPE('',$,#6783);
#6754=SHAPE_REPRESENTATION('',(#4131),#6627);
#6765=PRODUCT_DEFINITION_CONTEXT('part definition',#6851,'design');
#6783=PRODUCT_DEFINITION('M5x14 Cap Screw','M5x14 Cap Screw',#6811,#6765);
#6811=PRODUCT_DEFINITION_FORMATION('',$,#6870);
#6851=APPLICATION_CONTEXT(
'Core Data for Automotive Mechanical Design Process');
#6852=PRODUCT_CONTEXT('part definition',#6851,'mechanical');
#6870=PRODUCT('M5x14 Cap Screw','M5x14 Cap Screw','M5x14 Cap Screw',(#6852));
#6944=COLOUR_RGB('Black',0.12,0.14,0.17);
#6945=FILL_AREA_STYLE_COLOUR('',#6944);
#6946=FILL_AREA_STYLE('',(#6945));
#6947=SURFACE_STYLE_FILL_AREA(#6946);
#6948=SURFACE_SIDE_STYLE('',(#6947));
#6949=SURFACE_STYLE_USAGE(.BOTH.,#6948);
#6950=PRESENTATION_STYLE_ASSIGNMENT((#6949));
ENDSEC;
END-ISO-10303-21;
